ISO-10303-21;
HEADER;
/* Generated by software containing ST-Developer
 * from STEP Tools, Inc. (www.steptools.com) 
 */

FILE_DESCRIPTION(
/* description */ ('Shaft runout checking stand'),
/* implementation_level */ '2;1');

FILE_NAME(
/* name */ 'Roller support (1).step',
/* time_stamp */ '2026-11-02T21:12:33-08:00',
/* author */ (''),
/* organization */ (''),
/* preprocessor_version */ 'ST-DEVELOPER v20.2',
/* originating_system */ 'Autodesk Translation Framework v15.17.0.0',
/* authorisation */ '');

FILE_SCHEMA (('AUTOMOTIVE_DESIGN { 1 0 10303 214 3 1 1 }'));
ENDSEC;

DATA;
#10=MECHANICAL_DESIGN_GEOMETRIC_PRESENTATION_REPRESENTATION('',(#477),#11748);
#391=SHAPE_REPRESENTATION_RELATIONSHIP('SRR','None',#11940,#434);
#434=ADVANCED_BREP_SHAPE_REPRESENTATION('',(#528),#11716);
#477=STYLED_ITEM('',(#12169),#528);
#528=MANIFOLD_SOLID_BREP('Body1',#6220);
#613=FACE_BOUND('',#1605,.T.);
#614=FACE_BOUND('',#1606,.T.);
#615=FACE_BOUND('',#1611,.T.);
#616=FACE_BOUND('',#1612,.T.);
#617=FACE_BOUND('',#1616,.T.);
#618=FACE_BOUND('',#1617,.T.);
#619=FACE_BOUND('',#1621,.T.);
#620=FACE_BOUND('',#1622,.T.);
#750=CIRCLE('',#6975,0.33);
#751=CIRCLE('',#6976,0.33);
#752=CIRCLE('',#6978,0.33);
#753=CIRCLE('',#6979,0.33);
#754=CIRCLE('',#6981,1.1);
#755=CIRCLE('',#6982,1.1);
#756=CIRCLE('',#6984,0.5);
#757=CIRCLE('',#6985,0.5);
#758=CIRCLE('',#6988,0.5);
#759=CIRCLE('',#6990,0.5);
#975=CYLINDRICAL_SURFACE('',#6974,0.33);
#976=CYLINDRICAL_SURFACE('',#6977,0.33);
#977=CYLINDRICAL_SURFACE('',#6980,1.1);
#978=CYLINDRICAL_SURFACE('',#6987,0.5);
#979=CYLINDRICAL_SURFACE('',#6989,0.5);
#1182=FACE_OUTER_BOUND('',#1601,.T.);
#1183=FACE_OUTER_BOUND('',#1602,.T.);
#1184=FACE_OUTER_BOUND('',#1603,.T.);
#1185=FACE_OUTER_BOUND('',#1604,.T.);
#1186=FACE_OUTER_BOUND('',#1607,.T.);
#1187=FACE_OUTER_BOUND('',#1608,.T.);
#1188=FACE_OUTER_BOUND('',#1609,.T.);
#1189=FACE_OUTER_BOUND('',#1610,.T.);
#1190=FACE_OUTER_BOUND('',#1613,.T.);
#1191=FACE_OUTER_BOUND('',#1614,.T.);
#1192=FACE_OUTER_BOUND('',#1615,.T.);
#1193=FACE_OUTER_BOUND('',#1618,.T.);
#1194=FACE_OUTER_BOUND('',#1619,.T.);
#1195=FACE_OUTER_BOUND('',#1620,.T.);
#1601=EDGE_LOOP('',(#4764,#4765,#4766,#4767));
#1602=EDGE_LOOP('',(#4768,#4769,#4770,#4771));
#1603=EDGE_LOOP('',(#4772,#4773,#4774,#4775));
#1604=EDGE_LOOP('',(#4776,#4777,#4778,#4779,#4780,#4781));
#1605=EDGE_LOOP('',(#4782));
#1606=EDGE_LOOP('',(#4783));
#1607=EDGE_LOOP('',(#4784,#4785,#4786,#4787));
#1608=EDGE_LOOP('',(#4788,#4789,#4790,#4791));
#1609=EDGE_LOOP('',(#4792,#4793,#4794,#4795));
#1610=EDGE_LOOP('',(#4796,#4797,#4798,#4799));
#1611=EDGE_LOOP('',(#4800));
#1612=EDGE_LOOP('',(#4801));
#1613=EDGE_LOOP('',(#4802,#4803,#4804,#4805));
#1614=EDGE_LOOP('',(#4806,#4807,#4808,#4809,#4810,#4811));
#1615=EDGE_LOOP('',(#4812,#4813,#4814,#4815,#4816,#4817));
#1616=EDGE_LOOP('',(#4818));
#1617=EDGE_LOOP('',(#4819));
#1618=EDGE_LOOP('',(#4820,#4821,#4822,#4823,#4824,#4825));
#1619=EDGE_LOOP('',(#4826,#4827,#4828,#4829));
#1620=EDGE_LOOP('',(#4830,#4831,#4832,#4833));
#1621=EDGE_LOOP('',(#4834));
#1622=EDGE_LOOP('',(#4835));
#2144=LINE('',#10203,#2611);
#2145=LINE('',#10209,#2612);
#2146=LINE('',#10216,#2613);
#2147=LINE('',#10219,#2614);
#2148=LINE('',#10222,#2615);
#2149=LINE('',#10224,#2616);
#2150=LINE('',#10226,#2617);
#2151=LINE('',#10228,#2618);
#2152=LINE('',#10229,#2619);
#2153=LINE('',#10236,#2620);
#2154=LINE('',#10237,#2621);
#2155=LINE('',#10241,#2622);
#2156=LINE('',#10245,#2623);
#2157=LINE('',#10249,#2624);
#2158=LINE('',#10251,#2625);
#2159=LINE('',#10253,#2626);
#2160=LINE('',#10254,#2627);
#2161=LINE('',#10257,#2628);
#2162=LINE('',#10259,#2629);
#2163=LINE('',#10260,#2630);
#2164=LINE('',#10262,#2631);
#2165=LINE('',#10263,#2632);
#2166=LINE('',#10266,#2633);
#2167=LINE('',#10267,#2634);
#2168=LINE('',#10269,#2635);
#2169=LINE('',#10270,#2636);
#2611=VECTOR('',#8235,0.33);
#2612=VECTOR('',#8242,0.33);
#2613=VECTOR('',#8249,1.);
#2614=VECTOR('',#8252,1.);
#2615=VECTOR('',#8255,1.);
#2616=VECTOR('',#8256,1.);
#2617=VECTOR('',#8257,1.);
#2618=VECTOR('',#8258,1.);
#2619=VECTOR('',#8259,1.);
#2620=VECTOR('',#8266,1.);
#2621=VECTOR('',#8267,1.);
#2622=VECTOR('',#8272,0.5);
#2623=VECTOR('',#8277,0.5);
#2624=VECTOR('',#8280,1.);
#2625=VECTOR('',#8281,1.);
#2626=VECTOR('',#8282,1.);
#2627=VECTOR('',#8283,1.);
#2628=VECTOR('',#8286,1.);
#2629=VECTOR('',#8287,1.);
#2630=VECTOR('',#8288,1.);
#2631=VECTOR('',#8291,1.);
#2632=VECTOR('',#8292,1.);
#2633=VECTOR('',#8295,1.);
#2634=VECTOR('',#8296,1.);
#2635=VECTOR('',#8299,1.);
#2636=VECTOR('',#8300,1.);
#3044=VERTEX_POINT('',#10200);
#3045=VERTEX_POINT('',#10202);
#3046=VERTEX_POINT('',#10206);
#3047=VERTEX_POINT('',#10208);
#3048=VERTEX_POINT('',#10212);
#3049=VERTEX_POINT('',#10213);
#3050=VERTEX_POINT('',#10215);
#3051=VERTEX_POINT('',#10217);
#3052=VERTEX_POINT('',#10221);
#3053=VERTEX_POINT('',#10223);
#3054=VERTEX_POINT('',#10225);
#3055=VERTEX_POINT('',#10227);
#3056=VERTEX_POINT('',#10230);
#3057=VERTEX_POINT('',#10232);
#3058=VERTEX_POINT('',#10235);
#3059=VERTEX_POINT('',#10239);
#3060=VERTEX_POINT('',#10243);
#3061=VERTEX_POINT('',#10247);
#3062=VERTEX_POINT('',#10248);
#3063=VERTEX_POINT('',#10250);
#3064=VERTEX_POINT('',#10252);
#3065=VERTEX_POINT('',#10256);
#3066=VERTEX_POINT('',#10258);
#3067=VERTEX_POINT('',#10265);
#3668=EDGE_CURVE('',#3044,#3044,#750,.T.);
#3669=EDGE_CURVE('',#3044,#3045,#2144,.T.);
#3670=EDGE_CURVE('',#3045,#3045,#751,.T.);
#3671=EDGE_CURVE('',#3046,#3046,#752,.T.);
#3672=EDGE_CURVE('',#3046,#3047,#2145,.T.);
#3673=EDGE_CURVE('',#3047,#3047,#753,.T.);
#3674=EDGE_CURVE('',#3048,#3049,#754,.T.);
#3675=EDGE_CURVE('',#3050,#3048,#2146,.T.);
#3676=EDGE_CURVE('',#3051,#3050,#755,.T.);
#3677=EDGE_CURVE('',#3049,#3051,#2147,.T.);
#3678=EDGE_CURVE('',#3052,#3050,#2148,.T.);
#3679=EDGE_CURVE('',#3053,#3052,#2149,.T.);
#3680=EDGE_CURVE('',#3053,#3054,#2150,.T.);
#3681=EDGE_CURVE('',#3054,#3055,#2151,.T.);
#3682=EDGE_CURVE('',#3051,#3055,#2152,.T.);
#3683=EDGE_CURVE('',#3056,#3056,#756,.T.);
#3684=EDGE_CURVE('',#3057,#3057,#757,.T.);
#3685=EDGE_CURVE('',#3048,#3058,#2153,.T.);
#3686=EDGE_CURVE('',#3058,#3052,#2154,.T.);
#3687=EDGE_CURVE('',#3059,#3059,#758,.T.);
#3688=EDGE_CURVE('',#3059,#3057,#2155,.T.);
#3689=EDGE_CURVE('',#3060,#3060,#759,.T.);
#3690=EDGE_CURVE('',#3060,#3056,#2156,.T.);
#3691=EDGE_CURVE('',#3061,#3062,#2157,.T.);
#3692=EDGE_CURVE('',#3061,#3063,#2158,.T.);
#3693=EDGE_CURVE('',#3064,#3063,#2159,.T.);
#3694=EDGE_CURVE('',#3062,#3064,#2160,.T.);
#3695=EDGE_CURVE('',#3062,#3065,#2161,.T.);
#3696=EDGE_CURVE('',#3065,#3066,#2162,.T.);
#3697=EDGE_CURVE('',#3066,#3061,#2163,.T.);
#3698=EDGE_CURVE('',#3066,#3053,#2164,.T.);
#3699=EDGE_CURVE('',#3063,#3058,#2165,.T.);
#3700=EDGE_CURVE('',#3067,#3049,#2166,.T.);
#3701=EDGE_CURVE('',#3064,#3067,#2167,.T.);
#3702=EDGE_CURVE('',#3054,#3065,#2168,.T.);
#3703=EDGE_CURVE('',#3055,#3067,#2169,.T.);
#4764=ORIENTED_EDGE('',*,*,#3668,.F.);
#4765=ORIENTED_EDGE('',*,*,#3669,.T.);
#4766=ORIENTED_EDGE('',*,*,#3670,.F.);
#4767=ORIENTED_EDGE('',*,*,#3669,.F.);
#4768=ORIENTED_EDGE('',*,*,#3671,.F.);
#4769=ORIENTED_EDGE('',*,*,#3672,.T.);
#4770=ORIENTED_EDGE('',*,*,#3673,.F.);
#4771=ORIENTED_EDGE('',*,*,#3672,.F.);
#4772=ORIENTED_EDGE('',*,*,#3674,.F.);
#4773=ORIENTED_EDGE('',*,*,#3675,.F.);
#4774=ORIENTED_EDGE('',*,*,#3676,.F.);
#4775=ORIENTED_EDGE('',*,*,#3677,.F.);
#4776=ORIENTED_EDGE('',*,*,#3676,.T.);
#4777=ORIENTED_EDGE('',*,*,#3678,.F.);
#4778=ORIENTED_EDGE('',*,*,#3679,.F.);
#4779=ORIENTED_EDGE('',*,*,#3680,.T.);
#4780=ORIENTED_EDGE('',*,*,#3681,.T.);
#4781=ORIENTED_EDGE('',*,*,#3682,.F.);
#4782=ORIENTED_EDGE('',*,*,#3683,.T.);
#4783=ORIENTED_EDGE('',*,*,#3684,.T.);
#4784=ORIENTED_EDGE('',*,*,#3675,.T.);
#4785=ORIENTED_EDGE('',*,*,#3685,.T.);
#4786=ORIENTED_EDGE('',*,*,#3686,.T.);
#4787=ORIENTED_EDGE('',*,*,#3678,.T.);
#4788=ORIENTED_EDGE('',*,*,#3687,.F.);
#4789=ORIENTED_EDGE('',*,*,#3688,.T.);
#4790=ORIENTED_EDGE('',*,*,#3684,.F.);
#4791=ORIENTED_EDGE('',*,*,#3688,.F.);
#4792=ORIENTED_EDGE('',*,*,#3689,.F.);
#4793=ORIENTED_EDGE('',*,*,#3690,.T.);
#4794=ORIENTED_EDGE('',*,*,#3683,.F.);
#4795=ORIENTED_EDGE('',*,*,#3690,.F.);
#4796=ORIENTED_EDGE('',*,*,#3691,.F.);
#4797=ORIENTED_EDGE('',*,*,#3692,.T.);
#4798=ORIENTED_EDGE('',*,*,#3693,.F.);
#4799=ORIENTED_EDGE('',*,*,#3694,.F.);
#4800=ORIENTED_EDGE('',*,*,#3670,.T.);
#4801=ORIENTED_EDGE('',*,*,#3673,.T.);
#4802=ORIENTED_EDGE('',*,*,#3691,.T.);
#4803=ORIENTED_EDGE('',*,*,#3695,.T.);
#4804=ORIENTED_EDGE('',*,*,#3696,.T.);
#4805=ORIENTED_EDGE('',*,*,#3697,.T.);
#4806=ORIENTED_EDGE('',*,*,#3698,.T.);
#4807=ORIENTED_EDGE('',*,*,#3679,.T.);
#4808=ORIENTED_EDGE('',*,*,#3686,.F.);
#4809=ORIENTED_EDGE('',*,*,#3699,.F.);
#4810=ORIENTED_EDGE('',*,*,#3692,.F.);
#4811=ORIENTED_EDGE('',*,*,#3697,.F.);
#4812=ORIENTED_EDGE('',*,*,#3674,.T.);
#4813=ORIENTED_EDGE('',*,*,#3700,.F.);
#4814=ORIENTED_EDGE('',*,*,#3701,.F.);
#4815=ORIENTED_EDGE('',*,*,#3693,.T.);
#4816=ORIENTED_EDGE('',*,*,#3699,.T.);
#4817=ORIENTED_EDGE('',*,*,#3685,.F.);
#4818=ORIENTED_EDGE('',*,*,#3687,.T.);
#4819=ORIENTED_EDGE('',*,*,#3689,.T.);
#4820=ORIENTED_EDGE('',*,*,#3702,.T.);
#4821=ORIENTED_EDGE('',*,*,#3695,.F.);
#4822=ORIENTED_EDGE('',*,*,#3694,.T.);
#4823=ORIENTED_EDGE('',*,*,#3701,.T.);
#4824=ORIENTED_EDGE('',*,*,#3703,.F.);
#4825=ORIENTED_EDGE('',*,*,#3681,.F.);
#4826=ORIENTED_EDGE('',*,*,#3677,.T.);
#4827=ORIENTED_EDGE('',*,*,#3682,.T.);
#4828=ORIENTED_EDGE('',*,*,#3703,.T.);
#4829=ORIENTED_EDGE('',*,*,#3700,.T.);
#4830=ORIENTED_EDGE('',*,*,#3702,.F.);
#4831=ORIENTED_EDGE('',*,*,#3680,.F.);
#4832=ORIENTED_EDGE('',*,*,#3698,.F.);
#4833=ORIENTED_EDGE('',*,*,#3696,.F.);
#4834=ORIENTED_EDGE('',*,*,#3668,.T.);
#4835=ORIENTED_EDGE('',*,*,#3671,.T.);
#5710=PLANE('',#6983);
#5711=PLANE('',#6986);
#5712=PLANE('',#6991);
#5713=PLANE('',#6992);
#5714=PLANE('',#6993);
#5715=PLANE('',#6994);
#5716=PLANE('',#6995);
#5717=PLANE('',#6996);
#5718=PLANE('',#6997);
#5982=ADVANCED_FACE('',(#1182),#975,.F.);
#5983=ADVANCED_FACE('',(#1183),#976,.F.);
#5984=ADVANCED_FACE('',(#1184),#977,.F.);
#5985=ADVANCED_FACE('',(#1185,#613,#614),#5710,.T.);
#5986=ADVANCED_FACE('',(#1186),#5711,.T.);
#5987=ADVANCED_FACE('',(#1187),#978,.F.);
#5988=ADVANCED_FACE('',(#1188),#979,.F.);
#5989=ADVANCED_FACE('',(#1189,#615,#616),#5712,.T.);
#5990=ADVANCED_FACE('',(#1190),#5713,.F.);
#5991=ADVANCED_FACE('',(#1191),#5714,.T.);
#5992=ADVANCED_FACE('',(#1192,#617,#618),#5715,.T.);
#5993=ADVANCED_FACE('',(#1193),#5716,.T.);
#5994=ADVANCED_FACE('',(#1194),#5717,.T.);
#5995=ADVANCED_FACE('',(#1195,#619,#620),#5718,.F.);
#6220=CLOSED_SHELL('',(#5982,#5983,#5984,#5985,#5986,#5987,#5988,#5989,
#5990,#5991,#5992,#5993,#5994,#5995));
#6973=AXIS2_PLACEMENT_3D('',#10198,#8229,#8230);
#6974=AXIS2_PLACEMENT_3D('',#10199,#8231,#8232);
#6975=AXIS2_PLACEMENT_3D('',#10201,#8233,#8234);
#6976=AXIS2_PLACEMENT_3D('',#10204,#8236,#8237);
#6977=AXIS2_PLACEMENT_3D('',#10205,#8238,#8239);
#6978=AXIS2_PLACEMENT_3D('',#10207,#8240,#8241);
#6979=AXIS2_PLACEMENT_3D('',#10210,#8243,#8244);
#6980=AXIS2_PLACEMENT_3D('',#10211,#8245,#8246);
#6981=AXIS2_PLACEMENT_3D('',#10214,#8247,#8248);
#6982=AXIS2_PLACEMENT_3D('',#10218,#8250,#8251);
#6983=AXIS2_PLACEMENT_3D('',#10220,#8253,#8254);
#6984=AXIS2_PLACEMENT_3D('',#10231,#8260,#8261);
#6985=AXIS2_PLACEMENT_3D('',#10233,#8262,#8263);
#6986=AXIS2_PLACEMENT_3D('',#10234,#8264,#8265);
#6987=AXIS2_PLACEMENT_3D('',#10238,#8268,#8269);
#6988=AXIS2_PLACEMENT_3D('',#10240,#8270,#8271);
#6989=AXIS2_PLACEMENT_3D('',#10242,#8273,#8274);
#6990=AXIS2_PLACEMENT_3D('',#10244,#8275,#8276);
#6991=AXIS2_PLACEMENT_3D('',#10246,#8278,#8279);
#6992=AXIS2_PLACEMENT_3D('',#10255,#8284,#8285);
#6993=AXIS2_PLACEMENT_3D('',#10261,#8289,#8290);
#6994=AXIS2_PLACEMENT_3D('',#10264,#8293,#8294);
#6995=AXIS2_PLACEMENT_3D('',#10268,#8297,#8298);
#6996=AXIS2_PLACEMENT_3D('',#10271,#8301,#8302);
#6997=AXIS2_PLACEMENT_3D('',#10272,#8303,#8304);
#8229=DIRECTION('axis',(0.,0.,1.));
#8230=DIRECTION('refdir',(1.,0.,0.));
#8231=DIRECTION('center_axis',(0.,0.,1.));
#8232=DIRECTION('ref_axis',(1.,0.,0.));
#8233=DIRECTION('center_axis',(0.,0.,1.));
#8234=DIRECTION('ref_axis',(1.,0.,0.));
#8235=DIRECTION('',(0.,0.,1.));
#8236=DIRECTION('center_axis',(0.,0.,-1.));
#8237=DIRECTION('ref_axis',(1.,0.,0.));
#8238=DIRECTION('center_axis',(0.,0.,1.));
#8239=DIRECTION('ref_axis',(1.,0.,0.));
#8240=DIRECTION('center_axis',(0.,0.,1.));
#8241=DIRECTION('ref_axis',(1.,0.,0.));
#8242=DIRECTION('',(0.,0.,1.));
#8243=DIRECTION('center_axis',(0.,0.,-1.));
#8244=DIRECTION('ref_axis',(1.,0.,0.));
#8245=DIRECTION('center_axis',(0.,1.,0.));
#8246=DIRECTION('ref_axis',(1.,0.,0.));
#8247=DIRECTION('center_axis',(0.,1.,0.));
#8248=DIRECTION('ref_axis',(1.,0.,0.));
#8249=DIRECTION('',(0.,-1.,0.));
#8250=DIRECTION('center_axis',(0.,-1.,0.));
#8251=DIRECTION('ref_axis',(1.,0.,0.));
#8252=DIRECTION('',(0.,1.,0.));
#8253=DIRECTION('center_axis',(0.,1.,0.));
#8254=DIRECTION('ref_axis',(-1.,0.,0.));
#8255=DIRECTION('',(-1.,0.,0.));
#8256=DIRECTION('',(0.,0.,1.));
#8257=DIRECTION('',(-1.,0.,0.));
#8258=DIRECTION('',(0.,0.,1.));
#8259=DIRECTION('',(-1.,0.,0.));
#8260=DIRECTION('center_axis',(0.,-1.,0.));
#8261=DIRECTION('ref_axis',(1.,0.,0.));
#8262=DIRECTION('center_axis',(0.,-1.,0.));
#8263=DIRECTION('ref_axis',(1.,0.,0.));
#8264=DIRECTION('center_axis',(0.,0.,1.));
#8265=DIRECTION('ref_axis',(1.,0.,0.));
#8266=DIRECTION('',(1.,0.,0.));
#8267=DIRECTION('',(0.,1.,0.));
#8268=DIRECTION('center_axis',(0.,1.,0.));
#8269=DIRECTION('ref_axis',(1.,0.,0.));
#8270=DIRECTION('center_axis',(0.,1.,0.));
#8271=DIRECTION('ref_axis',(1.,0.,0.));
#8272=DIRECTION('',(0.,1.,0.));
#8273=DIRECTION('center_axis',(0.,1.,0.));
#8274=DIRECTION('ref_axis',(1.,0.,0.));
#8275=DIRECTION('center_axis',(0.,1.,0.));
#8276=DIRECTION('ref_axis',(1.,0.,0.));
#8277=DIRECTION('',(0.,1.,0.));
#8278=DIRECTION('center_axis',(0.,0.,1.));
#8279=DIRECTION('ref_axis',(1.,0.,0.));
#8280=DIRECTION('',(-1.,0.,0.));
#8281=DIRECTION('',(0.,1.,0.));
#8282=DIRECTION('',(1.,0.,0.));
#8283=DIRECTION('',(0.,1.,0.));
#8284=DIRECTION('center_axis',(0.,1.,0.));
#8285=DIRECTION('ref_axis',(1.,0.,0.));
#8286=DIRECTION('',(0.,0.,-1.));
#8287=DIRECTION('',(1.,0.,0.));
#8288=DIRECTION('',(0.,0.,1.));
#8289=DIRECTION('center_axis',(1.,0.,0.));
#8290=DIRECTION('ref_axis',(0.,1.,0.));
#8291=DIRECTION('',(0.,1.,0.));
#8292=DIRECTION('',(0.,0.,1.));
#8293=DIRECTION('center_axis',(0.,-1.,0.));
#8294=DIRECTION('ref_axis',(1.,0.,0.));
#8295=DIRECTION('',(1.,0.,0.));
#8296=DIRECTION('',(0.,0.,1.));
#8297=DIRECTION('center_axis',(-1.,0.,0.));
#8298=DIRECTION('ref_axis',(0.,-1.,0.));
#8299=DIRECTION('',(0.,-1.,0.));
#8300=DIRECTION('',(0.,-1.,0.));
#8301=DIRECTION('center_axis',(0.,0.,1.));
#8302=DIRECTION('ref_axis',(1.,0.,0.));
#8303=DIRECTION('center_axis',(0.,0.,1.));
#8304=DIRECTION('ref_axis',(1.,0.,0.));
#10198=CARTESIAN_POINT('',(0.,0.,0.));
#10199=CARTESIAN_POINT('Origin',(-3.5,7.5,2.7));
#10200=CARTESIAN_POINT('',(-3.83,7.5,2.8));
#10201=CARTESIAN_POINT('Origin',(-3.5,7.5,2.8));
#10202=CARTESIAN_POINT('',(-3.83,7.5,3.8));
#10203=CARTESIAN_POINT('',(-3.83,7.5,2.7));
#10204=CARTESIAN_POINT('Origin',(-3.5,7.5,3.8));
#10205=CARTESIAN_POINT('Origin',(3.5,7.5,2.7));
#10206=CARTESIAN_POINT('',(3.17,7.5,2.8));
#10207=CARTESIAN_POINT('Origin',(3.5,7.5,2.8));
#10208=CARTESIAN_POINT('',(3.17,7.5,3.8));
#10209=CARTESIAN_POINT('',(3.17,7.5,2.7));
#10210=CARTESIAN_POINT('Origin',(3.5,7.5,3.8));
#10211=CARTESIAN_POINT('Origin',(0.,8.4,6.95959179422654));
#10212=CARTESIAN_POINT('',(1.03956420750473,8.5,6.6));
#10213=CARTESIAN_POINT('',(-1.03956420750473,8.5,6.6));
#10214=CARTESIAN_POINT('Origin',(0.,8.5,6.95959179422654));
#10215=CARTESIAN_POINT('',(1.03956420750473,9.2,6.6));
#10216=CARTESIAN_POINT('',(1.03956420750473,8.4,6.6));
#10217=CARTESIAN_POINT('',(-1.03956420750473,9.2,6.6));
#10218=CARTESIAN_POINT('Origin',(0.,9.2,6.95959179422654));
#10219=CARTESIAN_POINT('',(-1.03956420750473,8.4,6.6));
#10220=CARTESIAN_POINT('Origin',(4.8,9.2,2.8));
#10221=CARTESIAN_POINT('',(4.8,9.2,6.6));
#10222=CARTESIAN_POINT('',(4.8,9.2,6.6));
#10223=CARTESIAN_POINT('',(4.8,9.2,2.8));
#10224=CARTESIAN_POINT('',(4.8,9.2,2.8));
#10225=CARTESIAN_POINT('',(-4.8,9.2,2.8));
#10226=CARTESIAN_POINT('',(4.8,9.2,2.8));
#10227=CARTESIAN_POINT('',(-4.8,9.2,6.6));
#10228=CARTESIAN_POINT('',(-4.8,9.2,2.8));
#10229=CARTESIAN_POINT('',(4.8,9.2,6.6));
#10230=CARTESIAN_POINT('',(1.5,9.2,5.));
#10231=CARTESIAN_POINT('Origin',(2.,9.2,5.));
#10232=CARTESIAN_POINT('',(-2.5,9.2,5.));
#10233=CARTESIAN_POINT('Origin',(-2.,9.2,5.));
#10234=CARTESIAN_POINT('Origin',(0.,8.85,6.6));
#10235=CARTESIAN_POINT('',(4.8,8.5,6.6));
#10236=CARTESIAN_POINT('',(-4.8,8.5,6.6));
#10237=CARTESIAN_POINT('',(4.8,8.5,6.6));
#10238=CARTESIAN_POINT('Origin',(-2.,8.4,5.));
#10239=CARTESIAN_POINT('',(-2.5,8.5,5.));
#10240=CARTESIAN_POINT('Origin',(-2.,8.5,5.));
#10241=CARTESIAN_POINT('',(-2.5,8.4,5.));
#10242=CARTESIAN_POINT('Origin',(2.,8.4,5.));
#10243=CARTESIAN_POINT('',(1.5,8.5,5.));
#10244=CARTESIAN_POINT('Origin',(2.,8.5,5.));
#10245=CARTESIAN_POINT('',(1.5,8.4,5.));
#10246=CARTESIAN_POINT('Origin',(-4.8,6.5,3.8));
#10247=CARTESIAN_POINT('',(4.8,6.5,3.8));
#10248=CARTESIAN_POINT('',(-4.8,6.5,3.8));
#10249=CARTESIAN_POINT('',(4.8,6.5,3.8));
#10250=CARTESIAN_POINT('',(4.8,8.5,3.8));
#10251=CARTESIAN_POINT('',(4.8,6.5,3.8));
#10252=CARTESIAN_POINT('',(-4.8,8.5,3.8));
#10253=CARTESIAN_POINT('',(-4.8,8.5,3.8));
#10254=CARTESIAN_POINT('',(-4.8,6.5,3.8));
#10255=CARTESIAN_POINT('Origin',(0.,6.5,3.3));
#10256=CARTESIAN_POINT('',(-4.8,6.5,2.8));
#10257=CARTESIAN_POINT('',(-4.8,6.5,3.8));
#10258=CARTESIAN_POINT('',(4.8,6.5,2.8));
#10259=CARTESIAN_POINT('',(-4.8,6.5,2.8));
#10260=CARTESIAN_POINT('',(4.8,6.5,2.8));
#10261=CARTESIAN_POINT('Origin',(4.8,8.5,2.8));
#10262=CARTESIAN_POINT('',(4.8,6.5,2.8));
#10263=CARTESIAN_POINT('',(4.8,8.5,2.8));
#10264=CARTESIAN_POINT('Origin',(-4.8,8.5,2.8));
#10265=CARTESIAN_POINT('',(-4.8,8.5,6.6));
#10266=CARTESIAN_POINT('',(-4.8,8.5,6.6));
#10267=CARTESIAN_POINT('',(-4.8,8.5,2.8));
#10268=CARTESIAN_POINT('Origin',(-4.8,9.2,2.8));
#10269=CARTESIAN_POINT('',(-4.8,9.2,2.8));
#10270=CARTESIAN_POINT('',(-4.8,9.2,6.6));
#10271=CARTESIAN_POINT('Origin',(0.,8.85,6.6));
#10272=CARTESIAN_POINT('Origin',(0.,8.85,2.8));
#11667=UNCERTAINTY_MEASURE_WITH_UNIT(LENGTH_MEASURE(0.001),#11749,
'DISTANCE_ACCURACY_VALUE',
'Maximum model space distance between geometric entities at asserted c
onnectivities');
#11699=UNCERTAINTY_MEASURE_WITH_UNIT(LENGTH_MEASURE(0.001),#11749,
'DISTANCE_ACCURACY_VALUE',
'Maximum model space distance between geometric entities at asserted c
onnectivities');
#11716=(
GEOMETRIC_REPRESENTATION_CONTEXT(3)
GLOBAL_UNCERTAINTY_ASSIGNED_CONTEXT((#11667))
GLOBAL_UNIT_ASSIGNED_CONTEXT((#11749,#11751,#11752))
REPRESENTATION_CONTEXT('','3D')
);
#11748=(
GEOMETRIC_REPRESENTATION_CONTEXT(3)
GLOBAL_UNCERTAINTY_ASSIGNED_CONTEXT((#11699))
GLOBAL_UNIT_ASSIGNED_CONTEXT((#11749,#11751,#11752))
REPRESENTATION_CONTEXT('','3D')
);
#11749=(
LENGTH_UNIT()
NAMED_UNIT(*)
SI_UNIT(.CENTI.,.METRE.)
);
#11751=(
NAMED_UNIT(*)
PLANE_ANGLE_UNIT()
SI_UNIT($,.RADIAN.)
);
#11752=(
NAMED_UNIT(*)
SI_UNIT($,.STERADIAN.)
SOLID_ANGLE_UNIT()
);
#11769=SHAPE_DEFINITION_REPRESENTATION(#11817,#11940);
#11817=PRODUCT_DEFINITION_SHAPE('',$,#11989);
#11940=SHAPE_REPRESENTATION('',(#6973),#11716);
#11972=PRODUCT_DEFINITION_CONTEXT('part definition',#12118,'design');
#11989=PRODUCT_DEFINITION('Roller support_1','Roller support (1)',#12037,
#11972);
#12037=PRODUCT_DEFINITION_FORMATION('',$,#12136);
#12118=APPLICATION_CONTEXT(
'Core Data for Automotive Mechanical Design Process');
#12119=PRODUCT_CONTEXT('part definition',#12118,'mechanical');
#12136=PRODUCT('Roller support_1','Roller support (1)','Roller support',
(#12119));
#12169=PRESENTATION_STYLE_ASSIGNMENT((#12174));
#12174=SURFACE_STYLE_USAGE(.BOTH.,#12179);
#12179=SURFACE_SIDE_STYLE('',(#12184));
#12184=SURFACE_STYLE_FILL_AREA(#12189);
#12189=FILL_AREA_STYLE('CAD Library Painted - Engineering blue',(#12194));
#12194=FILL_AREA_STYLE_COLOUR('CAD Library Painted - Engineering blue',
#12199);
#12199=COLOUR_RGB('CAD Library Painted - Engineering blue',0.12156862745098,
0.356862745098039,0.6);
ENDSEC;
END-ISO-10303-21;
